ISO-10303-21;
HEADER;
/* Generated by software containing ST-Developer
 * from STEP Tools, Inc. (www.steptools.com) 
 */

FILE_DESCRIPTION(
/* description */ ('Belt tension measurement rig'),
/* implementation_level */ '2;1');

FILE_NAME(
/* name */ 'Screw bushing (1).step',
/* time_stamp */ '2026-10-28T03:24:44-07:00',
/* author */ (''),
/* organization */ (''),
/* preprocessor_version */ 'ST-DEVELOPER v20.2',
/* originating_system */ 'Autodesk Translation Framework v15.17.0.0',
/* authorisation */ '');

FILE_SCHEMA (('AUTOMOTIVE_DESIGN { 1 0 10303 214 3 1 1 }'));
ENDSEC;

DATA;
#10=MECHANICAL_DESIGN_GEOMETRIC_PRESENTATION_REPRESENTATION('',(#702),#23587);
#592=SHAPE_REPRESENTATION_RELATIONSHIP('SRR','None',#23837,#647);
#647=ADVANCED_BREP_SHAPE_REPRESENTATION('',(#772),#23535);
#702=STYLED_ITEM('',(#24218),#772);
#772=MANIFOLD_SOLID_BREP('Body1',#12207);
#887=FACE_BOUND('',#2242,.T.);
#888=FACE_BOUND('',#2244,.T.);
#1105=PLANE('',#13134);
#1106=PLANE('',#13135);
#1477=FACE_OUTER_BOUND('',#2239,.T.);
#1478=FACE_OUTER_BOUND('',#2240,.T.);
#1479=FACE_OUTER_BOUND('',#2241,.T.);
#1480=FACE_OUTER_BOUND('',#2243,.T.);
#2239=EDGE_LOOP('',(#8448,#8449,#8450,#8451));
#2240=EDGE_LOOP('',(#8452,#8453,#8454,#8455));
#2241=EDGE_LOOP('',(#8456));
#2242=EDGE_LOOP('',(#8457));
#2243=EDGE_LOOP('',(#8458));
#2244=EDGE_LOOP('',(#8459));
#3109=LINE('',#19117,#3860);
#3110=LINE('',#19123,#3861);
#3860=VECTOR('',#15166,0.605);
#3861=VECTOR('',#15173,0.8);
#4584=CIRCLE('',#13129,0.605);
#4585=CIRCLE('',#13130,0.605);
#4586=CIRCLE('',#13132,0.8);
#4587=CIRCLE('',#13133,0.8);
#5408=VERTEX_POINT('',#19114);
#5409=VERTEX_POINT('',#19116);
#5410=VERTEX_POINT('',#19120);
#5411=VERTEX_POINT('',#19122);
#6583=EDGE_CURVE('',#5408,#5408,#4584,.T.);
#6584=EDGE_CURVE('',#5408,#5409,#3109,.T.);
#6585=EDGE_CURVE('',#5409,#5409,#4585,.T.);
#6586=EDGE_CURVE('',#5410,#5410,#4586,.T.);
#6587=EDGE_CURVE('',#5410,#5411,#3110,.T.);
#6588=EDGE_CURVE('',#5411,#5411,#4587,.T.);
#8448=ORIENTED_EDGE('',*,*,#6583,.F.);
#8449=ORIENTED_EDGE('',*,*,#6584,.T.);
#8450=ORIENTED_EDGE('',*,*,#6585,.T.);
#8451=ORIENTED_EDGE('',*,*,#6584,.F.);
#8452=ORIENTED_EDGE('',*,*,#6586,.F.);
#8453=ORIENTED_EDGE('',*,*,#6587,.T.);
#8454=ORIENTED_EDGE('',*,*,#6588,.T.);
#8455=ORIENTED_EDGE('',*,*,#6587,.F.);
#8456=ORIENTED_EDGE('',*,*,#6586,.T.);
#8457=ORIENTED_EDGE('',*,*,#6583,.T.);
#8458=ORIENTED_EDGE('',*,*,#6588,.F.);
#8459=ORIENTED_EDGE('',*,*,#6585,.F.);
#11215=CYLINDRICAL_SURFACE('',#13128,0.605);
#11216=CYLINDRICAL_SURFACE('',#13131,0.8);
#11618=ADVANCED_FACE('',(#1477),#11215,.F.);
#11619=ADVANCED_FACE('',(#1478),#11216,.T.);
#11620=ADVANCED_FACE('',(#1479,#887),#1105,.T.);
#11621=ADVANCED_FACE('',(#1480,#888),#1106,.F.);
#12207=CLOSED_SHELL('',(#11618,#11619,#11620,#11621));
#13127=AXIS2_PLACEMENT_3D('',#19112,#15160,#15161);
#13128=AXIS2_PLACEMENT_3D('',#19113,#15162,#15163);
#13129=AXIS2_PLACEMENT_3D('',#19115,#15164,#15165);
#13130=AXIS2_PLACEMENT_3D('',#19118,#15167,#15168);
#13131=AXIS2_PLACEMENT_3D('',#19119,#15169,#15170);
#13132=AXIS2_PLACEMENT_3D('',#19121,#15171,#15172);
#13133=AXIS2_PLACEMENT_3D('',#19124,#15174,#15175);
#13134=AXIS2_PLACEMENT_3D('',#19125,#15176,#15177);
#13135=AXIS2_PLACEMENT_3D('',#19126,#15178,#15179);
#15160=DIRECTION('axis',(0.,0.,1.));
#15161=DIRECTION('refdir',(1.,0.,0.));
#15162=DIRECTION('center_axis',(1.,0.,0.));
#15163=DIRECTION('ref_axis',(0.,0.,-1.));
#15164=DIRECTION('center_axis',(-1.,0.,0.));
#15165=DIRECTION('ref_axis',(0.,0.,-1.));
#15166=DIRECTION('',(-1.,0.,0.));
#15167=DIRECTION('center_axis',(-1.,0.,0.));
#15168=DIRECTION('ref_axis',(0.,0.,-1.));
#15169=DIRECTION('center_axis',(1.,0.,0.));
#15170=DIRECTION('ref_axis',(0.,0.,-1.));
#15171=DIRECTION('center_axis',(1.,0.,0.));
#15172=DIRECTION('ref_axis',(0.,0.,-1.));
#15173=DIRECTION('',(-1.,0.,0.));
#15174=DIRECTION('center_axis',(1.,0.,0.));
#15175=DIRECTION('ref_axis',(0.,0.,-1.));
#15176=DIRECTION('center_axis',(1.,0.,0.));
#15177=DIRECTION('ref_axis',(0.,0.,-1.));
#15178=DIRECTION('center_axis',(1.,0.,0.));
#15179=DIRECTION('ref_axis',(0.,0.,-1.));
#19112=CARTESIAN_POINT('',(0.,0.,0.));
#19113=CARTESIAN_POINT('Origin',(21.5,11.,4.5));
#19114=CARTESIAN_POINT('',(23.,11.,5.105));
#19115=CARTESIAN_POINT('Origin',(23.,11.,4.5));
#19116=CARTESIAN_POINT('',(21.5,11.,5.105));
#19117=CARTESIAN_POINT('',(21.5,11.,5.105));
#19118=CARTESIAN_POINT('Origin',(21.5,11.,4.5));
#19119=CARTESIAN_POINT('Origin',(21.5,11.,4.5));
#19120=CARTESIAN_POINT('',(23.,11.,5.3));
#19121=CARTESIAN_POINT('Origin',(23.,11.,4.5));
#19122=CARTESIAN_POINT('',(21.5,11.,5.3));
#19123=CARTESIAN_POINT('',(21.5,11.,5.3));
#19124=CARTESIAN_POINT('Origin',(21.5,11.,4.5));
#19125=CARTESIAN_POINT('Origin',(23.,11.,4.5));
#19126=CARTESIAN_POINT('Origin',(21.5,11.,4.5));
#23470=UNCERTAINTY_MEASURE_WITH_UNIT(LENGTH_MEASURE(0.001),#23588,
'DISTANCE_ACCURACY_VALUE',
'Maximum model space distance between geometric entities at asserted c
onnectivities');
#23522=UNCERTAINTY_MEASURE_WITH_UNIT(LENGTH_MEASURE(0.001),#23588,
'DISTANCE_ACCURACY_VALUE',
'Maximum model space distance between geometric entities at asserted c
onnectivities');
#23535=(
GEOMETRIC_REPRESENTATION_CONTEXT(3)
GLOBAL_UNCERTAINTY_ASSIGNED_CONTEXT((#23470))
GLOBAL_UNIT_ASSIGNED_CONTEXT((#23588,#23590,#23591))
REPRESENTATION_CONTEXT('','3D')
);
#23587=(
GEOMETRIC_REPRESENTATION_CONTEXT(3)
GLOBAL_UNCERTAINTY_ASSIGNED_CONTEXT((#23522))
GLOBAL_UNIT_ASSIGNED_CONTEXT((#23588,#23590,#23591))
REPRESENTATION_CONTEXT('','3D')
);
#23588=(
LENGTH_UNIT()
NAMED_UNIT(*)
SI_UNIT(.CENTI.,.METRE.)
);
#23590=(
NAMED_UNIT(*)
PLANE_ANGLE_UNIT()
SI_UNIT($,.RADIAN.)
);
#23591=(
NAMED_UNIT(*)
SI_UNIT($,.STERADIAN.)
SOLID_ANGLE_UNIT()
);
#23604=SHAPE_DEFINITION_REPRESENTATION(#23668,#23837);
#23668=PRODUCT_DEFINITION_SHAPE('',$,#23902);
#23837=SHAPE_REPRESENTATION('',(#13127),#23535);
#23889=PRODUCT_DEFINITION_CONTEXT('part definition',#24083,'design');
#23902=PRODUCT_DEFINITION('Screw bushing (1)','Screw bushing (1)',#23966,
#23889);
#23966=PRODUCT_DEFINITION_FORMATION('',$,#24097);
#24083=APPLICATION_CONTEXT(
'Core Data for Automotive Mechanical Design Process');
#24084=PRODUCT_CONTEXT('part definition',#24083,'mechanical');
#24097=PRODUCT('Screw bushing (1)','Screw bushing (1)','Screw bushing (1)',(#24084));
#24212=COLOUR_RGB('Black',0.12,0.14,0.17);
#24213=FILL_AREA_STYLE_COLOUR('',#24212);
#24214=FILL_AREA_STYLE('',(#24213));
#24215=SURFACE_STYLE_FILL_AREA(#24214);
#24216=SURFACE_SIDE_STYLE('',(#24215));
#24217=SURFACE_STYLE_USAGE(.BOTH.,#24216);
#24218=PRESENTATION_STYLE_ASSIGNMENT((#24217));
ENDSEC;
END-ISO-10303-21;
